ISO-10303-21;
HEADER;
FILE_DESCRIPTION (('STEP AP214'),
    '1' );
FILE_NAME ('Sleeve.step',
    '2026-10-22T18:53:08',
    ( '' ),
    ( '' ),
    'SwSTEP 2.0',
    'SolidWorks 2025',
    '' );
FILE_SCHEMA (( 'AUTOMOTIVE_DESIGN' ));
ENDSEC;

DATA;
#190=AXIS2_PLACEMENT_3D ( 'NONE', #9359, #5489, #18425 ) ;
#242=DIRECTION ( 'NONE',  ( 1.000000000000000000, 0.000000000000000000, 0.000000000000000000 ) ) ;
#407=EDGE_LOOP ( 'NONE', ( #9562, #5623, #18724, #2423 ) ) ;
#552=VECTOR ( 'NONE', #2265, 1000.000000000000114 ) ;
#661=AXIS2_PLACEMENT_3D ( 'NONE', #11705, #19548, #17347 ) ;
#675=EDGE_LOOP ( 'NONE', ( #20908, #21165, #3943, #19400 ) ) ;
#706=EDGE_LOOP ( 'NONE', ( #6726, #22975, #16577, #8092 ) ) ;
#831=VERTEX_POINT ( 'NONE', #23222 ) ;
#899=CARTESIAN_POINT ( 'NONE',  ( -9.999999999999998224, 0.000000000000000000, 15.50000000000000000 ) ) ;
#1216=ORIENTED_EDGE ( 'NONE', *, *, #15855, .T. ) ;
#1385=EDGE_LOOP ( 'NONE', ( #16104, #7716, #9103, #16213 ) ) ;
#1392=FACE_OUTER_BOUND ( 'NONE', #706, .T. ) ;
#1453=DIRECTION ( 'NONE',  ( -0.000000000000000000, -0.000000000000000000, -1.000000000000000000 ) ) ;
#1736=CARTESIAN_POINT ( 'NONE',  ( 0.000000000000000000, 0.000000000000000000, 15.50000000000000000 ) ) ;
#1882=EDGE_CURVE ( 'NONE', #16756, #20379, #21513, .T. ) ;
#1967=LINE ( 'NONE', #4303, #10378 ) ;
#2136=AXIS2_PLACEMENT_3D ( 'NONE', #14845, #22314, #5593 ) ;
#2153=DIRECTION ( 'NONE',  ( 1.000000000000000000, 0.000000000000000000, 0.000000000000000000 ) ) ;
#2265=DIRECTION ( 'NONE',  ( -0.7071067811865474617, 8.659560562354932858E-17, 0.7071067811865474617 ) ) ;
#2303=( NAMED_UNIT ( * ) SI_UNIT ( $, .STERADIAN. ) SOLID_ANGLE_UNIT ( ) );
#2414=AXIS2_PLACEMENT_3D ( 'NONE', #2606, #7943, #11853 ) ;
#2423=ORIENTED_EDGE ( 'NONE', *, *, #22502, .F. ) ;
#2437=CONICAL_SURFACE ( 'NONE', #18805, 9.000000000000000000, 0.7853981633974482790 ) ;
#2543=DIRECTION ( 'NONE',  ( -0.000000000000000000, -0.000000000000000000, -1.000000000000000000 ) ) ;
#2606=CARTESIAN_POINT ( 'NONE',  ( 0.000000000000000000, 0.000000000000000000, 15.00000000000000178 ) ) ;
#2778=CARTESIAN_POINT ( 'NONE',  ( 0.000000000000000000, 0.000000000000000000, 15.50000000000000000 ) ) ;
#3001=ADVANCED_FACE ( 'NONE', ( #20856 ), #21207, .F. ) ;
#3181=ORIENTED_EDGE ( 'NONE', *, *, #5669, .T. ) ;
#3234=APPLICATION_CONTEXT ( 'automotive_design' ) ;
#3329=DIRECTION ( 'NONE',  ( 0.000000000000000000, 0.000000000000000000, 1.000000000000000000 ) ) ;
#3369=ADVANCED_FACE ( 'NONE', ( #8681 ), #7221, .T. ) ;
#3461=CARTESIAN_POINT ( 'NONE',  ( -9.000000000000000000, 0.000000000000000000, 15.00000000000000178 ) ) ;
#3463=VERTEX_POINT ( 'NONE', #12763 ) ;
#3483=ADVANCED_BREP_SHAPE_REPRESENTATION ( '', ( #19017, #8005 ), #14253 ) ;
#3682=CARTESIAN_POINT ( 'NONE',  ( 0.000000000000000000, 0.000000000000000000, 15.00000000000000178 ) ) ;
#3690=ORIENTED_EDGE ( 'NONE', *, *, #23588, .F. ) ;
#3787=EDGE_LOOP ( 'NONE', ( #11016, #14336 ) ) ;
#3854=ORIENTED_EDGE ( 'NONE', *, *, #9226, .T. ) ;
#3943=ORIENTED_EDGE ( 'NONE', *, *, #19409, .T. ) ;
#4072=DIRECTION ( 'NONE',  ( 0.7071067811865474617, 0.000000000000000000, 0.7071067811865474617 ) ) ;
#4105=CARTESIAN_POINT ( 'NONE',  ( -9.000000000000000000, 1.102182119232617714E-15, 15.00000000000000178 ) ) ;
#4146=( NAMED_UNIT ( * ) PLANE_ANGLE_UNIT ( ) SI_UNIT ( $, .RADIAN. ) );
#4147=CYLINDRICAL_SURFACE ( 'NONE', #19590, 9.000000000000000000 ) ;
#4260=EDGE_CURVE ( 'NONE', #15663, #13780, #10089, .T. ) ;
#4303=CARTESIAN_POINT ( 'NONE',  ( 9.000000000000000000, 1.102182119232617714E-15, 15.50000000000000000 ) ) ;
#4342=DIRECTION ( 'NONE',  ( 0.7071067811865474617, 8.659560562354932858E-17, -0.7071067811865474617 ) ) ;
#4514=ORIENTED_EDGE ( 'NONE', *, *, #22502, .T. ) ;
#4535=CARTESIAN_POINT ( 'NONE',  ( -9.000000000000000000, 0.000000000000000000, 15.50000000000000000 ) ) ;
#4557=EDGE_LOOP ( 'NONE', ( #19858, #9592, #10653, #9340 ) ) ;
#4729=ADVANCED_FACE ( 'NONE', ( #12694, #22121 ), #20037, .F. ) ;
#4970=EDGE_CURVE ( 'NONE', #16756, #3463, #10291, .T. ) ;
#5127=CARTESIAN_POINT ( 'NONE',  ( 9.000000000000000000, 1.102182119232617714E-15, 0.4999999999999970024 ) ) ;
#5250=EDGE_CURVE ( 'NONE', #20068, #14422, #22016, .T. ) ;
#5289=DIRECTION ( 'NONE',  ( 1.000000000000000000, 0.000000000000000000, 0.000000000000000000 ) ) ;
#5300=EDGE_CURVE ( 'NONE', #13710, #831, #15765, .T. ) ;
#5389=CARTESIAN_POINT ( 'NONE',  ( 0.000000000000000000, 0.000000000000000000, 0.000000000000000000 ) ) ;
#5398=CYLINDRICAL_SURFACE ( 'NONE', #19263, 9.999999999999998224 ) ;
#5400=DIRECTION ( 'NONE',  ( -0.000000000000000000, -0.000000000000000000, -1.000000000000000000 ) ) ;
#5418=ORIENTED_EDGE ( 'NONE', *, *, #10368, .T. ) ;
#5489=DIRECTION ( 'NONE',  ( 0.000000000000000000, 0.000000000000000000, 1.000000000000000000 ) ) ;
#5575=VECTOR ( 'NONE', #4072, 1000.000000000000114 ) ;
#5591=ORIENTED_EDGE ( 'NONE', *, *, #4970, .T. ) ;
#5593=DIRECTION ( 'NONE',  ( 1.000000000000000000, 0.000000000000000000, -0.000000000000000000 ) ) ;
#5617=DIRECTION ( 'NONE',  ( -0.000000000000000000, -0.000000000000000000, -1.000000000000000000 ) ) ;
#5623=ORIENTED_EDGE ( 'NONE', *, *, #23588, .T. ) ;
#5669=EDGE_CURVE ( 'NONE', #16889, #20379, #23909, .T. ) ;
#5797=EDGE_CURVE ( 'NONE', #3463, #16889, #8926, .T. ) ;
#5837=DIRECTION ( 'NONE',  ( -0.000000000000000000, -0.000000000000000000, -1.000000000000000000 ) ) ;
#5911=( GEOMETRIC_REPRESENTATION_CONTEXT ( 3 ) GLOBAL_UNCERTAINTY_ASSIGNED_CONTEXT ( ( #17651 ) ) GLOBAL_UNIT_ASSIGNED_CONTEXT ( ( #22675, #4146, #2303 ) ) REPRESENTATION_CONTEXT ( 'NONE', 'WORKASPACE' ) );
#5966=DIRECTION ( 'NONE',  ( -0.000000000000000000, -0.000000000000000000, -1.000000000000000000 ) ) ;
#5978=CARTESIAN_POINT ( 'NONE',  ( 0.000000000000000000, 0.000000000000000000, 0.000000000000000000 ) ) ;
#6130=SHAPE_REPRESENTATION ( 'Sleeve', ( #8005 ), #14253 ) ;
#6141=DIRECTION ( 'NONE',  ( 1.000000000000000000, 0.000000000000000000, 0.000000000000000000 ) ) ;
#6173=AXIS2_PLACEMENT_3D ( 'NONE', #19327, #22871, #6141 ) ;
#6522=PRODUCT_DEFINITION_SHAPE ( 'NONE', 'NONE',  #13308 ) ;
#6726=ORIENTED_EDGE ( 'NONE', *, *, #16437, .F. ) ;
#7081=STYLED_ITEM('',(#24141),#19017);
#7221=CYLINDRICAL_SURFACE ( 'NONE', #17853, 9.999999999999998224 ) ;
#7407=FACE_OUTER_BOUND ( 'NONE', #1385, .T. ) ;
#7521=VECTOR ( 'NONE', #16622, 1000.000000000000000 ) ;
#7716=ORIENTED_EDGE ( 'NONE', *, *, #16437, .T. ) ;
#7943=DIRECTION ( 'NONE',  ( 0.000000000000000000, 0.000000000000000000, 1.000000000000000000 ) ) ;
#8005=AXIS2_PLACEMENT_3D ( 'NONE', #5978, #22344, #13412 ) ;
#8092=ORIENTED_EDGE ( 'NONE', *, *, #10368, .F. ) ;
#8096=EDGE_LOOP ( 'NONE', ( #3690, #20898, #4514, #23620 ) ) ;
#8116=EDGE_LOOP ( 'NONE', ( #16429, #18795, #3181, #19268 ) ) ;
#8126=UNCERTAINTY_MEASURE_WITH_UNIT (LENGTH_MEASURE( 1.000000000000000082E-05 ), #13162, 'distance_accuracy_value', 'NONE');
#8347=EDGE_CURVE ( 'NONE', #3463, #16756, #9424, .T. ) ;
#8659=AXIS2_PLACEMENT_3D ( 'NONE', #10082, #5837, #242 ) ;
#8681=FACE_OUTER_BOUND ( 'NONE', #8116, .T. ) ;
#8724=AXIS2_PLACEMENT_3D ( 'NONE', #15352, #22826, #21093 ) ;
#8832=CONICAL_SURFACE ( 'NONE', #661, 9.499999999999996447, 0.7853981633974482790 ) ;
#8875=EDGE_CURVE ( 'NONE', #831, #13710, #18407, .T. ) ;
#8926=LINE ( 'NONE', #11104, #7521 ) ;
#9037=DIRECTION ( 'NONE',  ( -1.000000000000000000, 0.000000000000000000, 0.000000000000000000 ) ) ;
#9103=ORIENTED_EDGE ( 'NONE', *, *, #5250, .F. ) ;
#9226=EDGE_CURVE ( 'NONE', #17379, #13080, #17633, .T. ) ;
#9244=FACE_OUTER_BOUND ( 'NONE', #11931, .T. ) ;
#9340=ORIENTED_EDGE ( 'NONE', *, *, #22861, .T. ) ;
#9359=CARTESIAN_POINT ( 'NONE',  ( 0.000000000000000000, 0.000000000000000000, 15.00000000000000178 ) ) ;
#9424=CIRCLE ( 'NONE', #19611, 9.999999999999998224 ) ;
#9536=VECTOR ( 'NONE', #12051, 1000.000000000000000 ) ;
#9561=SHAPE_DEFINITION_REPRESENTATION ( #6522, #6130 ) ;
#9562=ORIENTED_EDGE ( 'NONE', *, *, #19409, .F. ) ;
#9592=ORIENTED_EDGE ( 'NONE', *, *, #4970, .F. ) ;
#9610=DIRECTION ( 'NONE',  ( 1.000000000000000000, 0.000000000000000000, 0.000000000000000000 ) ) ;
#9646=CARTESIAN_POINT ( 'NONE',  ( -9.499999999999996447, 0.000000000000000000, 0.000000000000000000 ) ) ;
#9892=AXIS2_PLACEMENT_3D ( 'NONE', #5389, #10614, #18208 ) ;
#9936=VECTOR ( 'NONE', #16513, 1000.000000000000114 ) ;
#10082=CARTESIAN_POINT ( 'NONE',  ( 0.000000000000000000, 0.000000000000000000, 0.4999999999999970024 ) ) ;
#10089=CIRCLE ( 'NONE', #6173, 9.499999999999996447 ) ;
#10165=CARTESIAN_POINT ( 'NONE',  ( 9.499999999999996447, 1.163414459189985091E-15, 0.000000000000000000 ) ) ;
#10291=CIRCLE ( 'NONE', #8724, 9.999999999999998224 ) ;
#10368=EDGE_CURVE ( 'NONE', #14422, #20068, #18786, .T. ) ;
#10378=VECTOR ( 'NONE', #17346, 1000.000000000000000 ) ;
#10390=ADVANCED_FACE ( 'NONE', ( #17428 ), #4147, .F. ) ;
#10614=DIRECTION ( 'NONE',  ( 0.000000000000000000, 0.000000000000000000, 1.000000000000000000 ) ) ;
#10624=DIRECTION ( 'NONE',  ( -1.000000000000000000, 0.000000000000000000, 0.000000000000000000 ) ) ;
#10653=ORIENTED_EDGE ( 'NONE', *, *, #1882, .T. ) ;
#10672=AXIS2_PLACEMENT_3D ( 'NONE', #3682, #3329, #11094 ) ;
#11016=ORIENTED_EDGE ( 'NONE', *, *, #22861, .F. ) ;
#11094=DIRECTION ( 'NONE',  ( 1.000000000000000000, 0.000000000000000000, 0.000000000000000000 ) ) ;
#11104=CARTESIAN_POINT ( 'NONE',  ( 9.999999999999998224, 1.224646799147353059E-15, 15.50000000000000000 ) ) ;
#11121=CARTESIAN_POINT ( 'NONE',  ( -9.499999999999996447, 0.000000000000000000, 0.000000000000000000 ) ) ;
#11175=PLANE ( 'NONE',  #2136 ) ;
#11287=DIRECTION ( 'NONE',  ( 1.000000000000000000, 0.000000000000000000, 0.000000000000000000 ) ) ;
#11373=PRODUCT_CONTEXT ( 'NONE', #3234, 'mechanical' ) ;
#11585=VECTOR ( 'NONE', #21641, 1000.000000000000000 ) ;
#11660=DIRECTION ( 'NONE',  ( -1.000000000000000000, 0.000000000000000000, 0.000000000000000000 ) ) ;
#11705=CARTESIAN_POINT ( 'NONE',  ( 0.000000000000000000, 0.000000000000000000, 0.000000000000000000 ) ) ;
#11853=DIRECTION ( 'NONE',  ( 1.000000000000000000, 0.000000000000000000, 0.000000000000000000 ) ) ;
#11918=ADVANCED_FACE ( 'NONE', ( #7407 ), #2437, .F. ) ;
#11931=EDGE_LOOP ( 'NONE', ( #5591, #21895 ) ) ;
#12001=LINE ( 'NONE', #10165, #20122 ) ;
#12051=DIRECTION ( 'NONE',  ( -0.000000000000000000, -0.000000000000000000, -1.000000000000000000 ) ) ;
#12177=LINE ( 'NONE', #4535, #9536 ) ;
#12283=EDGE_CURVE ( 'NONE', #831, #20068, #13315, .T. ) ;
#12318=PRODUCT_DEFINITION_FORMATION_WITH_SPECIFIED_SOURCE ( 'ANY', '', #13924, .NOT_KNOWN. ) ;
#12505=FACE_OUTER_BOUND ( 'NONE', #8096, .T. ) ;
#12536=AXIS2_PLACEMENT_3D ( 'NONE', #18870, #13006, #2153 ) ;
#12694=FACE_BOUND ( 'NONE', #22841, .T. ) ;
#12709=CARTESIAN_POINT ( 'NONE',  ( -9.999999999999998224, 0.000000000000000000, 15.50000000000000000 ) ) ;
#12763=CARTESIAN_POINT ( 'NONE',  ( 9.999999999999998224, 1.224646799147353059E-15, 15.50000000000000000 ) ) ;
#12804=EDGE_LOOP ( 'NONE', ( #19777, #15106, #14825, #3854 ) ) ;
#12925=MECHANICAL_DESIGN_GEOMETRIC_PRESENTATION_REPRESENTATION('',(#7081),#5911);
#13006=DIRECTION ( 'NONE',  ( -0.000000000000000000, -0.000000000000000000, -1.000000000000000000 ) ) ;
#13042=DIRECTION ( 'NONE',  ( 1.000000000000000000, 0.000000000000000000, 0.000000000000000000 ) ) ;
#13080=VERTEX_POINT ( 'NONE', #5127 ) ;
#13086=LINE ( 'NONE', #11121, #9936 ) ;
#13162=( LENGTH_UNIT ( ) NAMED_UNIT ( * ) SI_UNIT ( .MILLI., .METRE. ) );
#13201=CARTESIAN_POINT ( 'NONE',  ( 9.000000000000000000, 0.000000000000000000, 15.00000000000000178 ) ) ;
#13279=SHAPE_REPRESENTATION_RELATIONSHIP ( 'NONE' , 'NONE' ,  #6130, #3483 ) ;
#13308=PRODUCT_DEFINITION ( 'UNKNOWN', '', #12318, #20922 ) ;
#13315=LINE ( 'NONE', #13201, #5575 ) ;
#13336=ORIENTED_EDGE ( 'NONE', *, *, #5250, .T. ) ;
#13410=CONICAL_SURFACE ( 'NONE', #10672, 9.000000000000000000, 0.7853981633974482790 ) ;
#13412=DIRECTION ( 'NONE',  ( 1.000000000000000000, 0.000000000000000000, 0.000000000000000000 ) ) ;
#13710=VERTEX_POINT ( 'NONE', #3461 ) ;
#13728=EDGE_CURVE ( 'NONE', #831, #13080, #1967, .T. ) ;
#13780=VERTEX_POINT ( 'NONE', #9646 ) ;
#13864=APPLICATION_CONTEXT ( 'automotive_design' ) ;
#13902=CARTESIAN_POINT ( 'NONE',  ( 0.000000000000000000, 0.000000000000000000, 15.50000000000000000 ) ) ;
#13924=PRODUCT ( 'Sleeve', 'Sleeve', '', ( #11373 ) ) ;
#14188=EDGE_CURVE ( 'NONE', #13710, #17379, #12177, .T. ) ;
#14218=CARTESIAN_POINT ( 'NONE',  ( -9.000000000000000000, 0.000000000000000000, 0.4999999999999970024 ) ) ;
#14253=( GEOMETRIC_REPRESENTATION_CONTEXT ( 3 ) GLOBAL_UNCERTAINTY_ASSIGNED_CONTEXT ( ( #8126 ) ) GLOBAL_UNIT_ASSIGNED_CONTEXT ( ( #13162, #17183, #14864 ) ) REPRESENTATION_CONTEXT ( 'NONE', 'WORKASPACE' ) );
#14298=DIRECTION ( 'NONE',  ( -0.000000000000000000, -0.000000000000000000, -1.000000000000000000 ) ) ;
#14336=ORIENTED_EDGE ( 'NONE', *, *, #5669, .F. ) ;
#14405=DIRECTION ( 'NONE',  ( 1.000000000000000000, 0.000000000000000000, 0.000000000000000000 ) ) ;
#14422=VERTEX_POINT ( 'NONE', #15675 ) ;
#14485=FACE_BOUND ( 'NONE', #15207, .T. ) ;
#14540=CIRCLE ( 'NONE', #20398, 9.499999999999996447 ) ;
#14825=ORIENTED_EDGE ( 'NONE', *, *, #14188, .T. ) ;
#14845=CARTESIAN_POINT ( 'NONE',  ( 0.000000000000000000, 0.000000000000000000, 15.50000000000000000 ) ) ;
#14849=DIRECTION ( 'NONE',  ( 0.000000000000000000, 0.000000000000000000, 1.000000000000000000 ) ) ;
#14864=( NAMED_UNIT ( * ) SI_UNIT ( $, .STERADIAN. ) SOLID_ANGLE_UNIT ( ) );
#14910=ADVANCED_FACE ( 'NONE', ( #14485, #9244 ), #11175, .T. ) ;
#14970=CARTESIAN_POINT ( 'NONE',  ( 0.000000000000000000, 0.000000000000000000, 15.00000000000000178 ) ) ;
#15098=CARTESIAN_POINT ( 'NONE',  ( 0.000000000000000000, 0.000000000000000000, 15.50000000000000000 ) ) ;
#15106=ORIENTED_EDGE ( 'NONE', *, *, #8875, .T. ) ;
#15207=EDGE_LOOP ( 'NONE', ( #13336, #5418 ) ) ;
#15352=CARTESIAN_POINT ( 'NONE',  ( 0.000000000000000000, 0.000000000000000000, 15.50000000000000000 ) ) ;
#15359=CARTESIAN_POINT ( 'NONE',  ( 9.499999999999996447, 1.163414459189985091E-15, 0.000000000000000000 ) ) ;
#15505=FACE_OUTER_BOUND ( 'NONE', #407, .T. ) ;
#15515=CLOSED_SHELL ( 'NONE', ( #11918, #23931, #3001, #3369, #14910, #4729, #16764, #10390, #16176, #16697 ) ) ;
#15663=VERTEX_POINT ( 'NONE', #15359 ) ;
#15675=CARTESIAN_POINT ( 'NONE',  ( -9.499999999999998224, 1.163414459189985288E-15, 15.50000000000000000 ) ) ;
#15765=CIRCLE ( 'NONE', #190, 9.000000000000000000 ) ;
#15855=EDGE_CURVE ( 'NONE', #13780, #15663, #14540, .T. ) ;
#16104=ORIENTED_EDGE ( 'NONE', *, *, #5300, .F. ) ;
#16122=CONICAL_SURFACE ( 'NONE', #18472, 9.499999999999996447, 0.7853981633974482790 ) ;
#16176=ADVANCED_FACE ( 'NONE', ( #12505 ), #16122, .F. ) ;
#16213=ORIENTED_EDGE ( 'NONE', *, *, #12283, .F. ) ;
#16301=DIRECTION ( 'NONE',  ( -1.000000000000000000, 0.000000000000000000, 0.000000000000000000 ) ) ;
#16366=DIRECTION ( 'NONE',  ( 0.000000000000000000, 0.000000000000000000, 1.000000000000000000 ) ) ;
#16429=ORIENTED_EDGE ( 'NONE', *, *, #8347, .F. ) ;
#16437=EDGE_CURVE ( 'NONE', #13710, #14422, #20943, .T. ) ;
#16513=DIRECTION ( 'NONE',  ( -0.7071067811865474617, 0.000000000000000000, -0.7071067811865474617 ) ) ;
#16577=ORIENTED_EDGE ( 'NONE', *, *, #12283, .T. ) ;
#16622=DIRECTION ( 'NONE',  ( -0.000000000000000000, -0.000000000000000000, -1.000000000000000000 ) ) ;
#16697=ADVANCED_FACE ( 'NONE', ( #1392 ), #13410, .F. ) ;
#16707=CARTESIAN_POINT ( 'NONE',  ( 0.000000000000000000, 0.000000000000000000, 15.50000000000000000 ) ) ;
#16756=VERTEX_POINT ( 'NONE', #12709 ) ;
#16764=ADVANCED_FACE ( 'NONE', ( #23712 ), #5398, .T. ) ;
#16889=VERTEX_POINT ( 'NONE', #22927 ) ;
#17183=( NAMED_UNIT ( * ) PLANE_ANGLE_UNIT ( ) SI_UNIT ( $, .RADIAN. ) );
#17346=DIRECTION ( 'NONE',  ( -0.000000000000000000, -0.000000000000000000, -1.000000000000000000 ) ) ;
#17347=DIRECTION ( 'NONE',  ( -1.000000000000000000, 0.000000000000000000, 0.000000000000000000 ) ) ;
#17365=CIRCLE ( 'NONE', #19334, 9.999999999999998224 ) ;
#17379=VERTEX_POINT ( 'NONE', #14218 ) ;
#17428=FACE_OUTER_BOUND ( 'NONE', #12804, .T. ) ;
#17633=CIRCLE ( 'NONE', #8659, 9.000000000000000000 ) ;
#17651=UNCERTAINTY_MEASURE_WITH_UNIT (LENGTH_MEASURE( 1.000000000000000082E-05 ), #22675, 'distance_accuracy_value', 'NONE');
#17853=AXIS2_PLACEMENT_3D ( 'NONE', #21761, #5400, #9037 ) ;
#18081=AXIS2_PLACEMENT_3D ( 'NONE', #23477, #16366, #5289 ) ;
#18116=AXIS2_PLACEMENT_3D ( 'NONE', #16707, #5617, #13042 ) ;
#18176=ORIENTED_EDGE ( 'NONE', *, *, #4260, .T. ) ;
#18208=DIRECTION ( 'NONE',  ( 1.000000000000000000, 0.000000000000000000, -0.000000000000000000 ) ) ;
#18407=CIRCLE ( 'NONE', #2414, 9.000000000000000000 ) ;
#18425=DIRECTION ( 'NONE',  ( 1.000000000000000000, 0.000000000000000000, 0.000000000000000000 ) ) ;
#18472=AXIS2_PLACEMENT_3D ( 'NONE', #19975, #1453, #16301 ) ;
#18666=CARTESIAN_POINT ( 'NONE',  ( 9.499999999999998224, 0.000000000000000000, 15.50000000000000000 ) ) ;
#18724=ORIENTED_EDGE ( 'NONE', *, *, #15855, .F. ) ;
#18786=CIRCLE ( 'NONE', #23858, 9.499999999999998224 ) ;
#18795=ORIENTED_EDGE ( 'NONE', *, *, #5797, .T. ) ;
#18805=AXIS2_PLACEMENT_3D ( 'NONE', #14970, #14849, #22318 ) ;
#18870=CARTESIAN_POINT ( 'NONE',  ( 0.000000000000000000, 0.000000000000000000, 0.4999999999999970024 ) ) ;
#19017=MANIFOLD_SOLID_BREP ( 'Chamfer1', #15515 ) ;
#19263=AXIS2_PLACEMENT_3D ( 'NONE', #1736, #14298, #10624 ) ;
#19268=ORIENTED_EDGE ( 'NONE', *, *, #1882, .F. ) ;
#19327=CARTESIAN_POINT ( 'NONE',  ( 0.000000000000000000, 0.000000000000000000, 0.000000000000000000 ) ) ;
#19334=AXIS2_PLACEMENT_3D ( 'NONE', #21391, #20042, #14405 ) ;
#19400=ORIENTED_EDGE ( 'NONE', *, *, #14188, .F. ) ;
#19409=EDGE_CURVE ( 'NONE', #13080, #17379, #21119, .T. ) ;
#19548=DIRECTION ( 'NONE',  ( -0.000000000000000000, -0.000000000000000000, -1.000000000000000000 ) ) ;
#19590=AXIS2_PLACEMENT_3D ( 'NONE', #21081, #23045, #22676 ) ;
#19611=AXIS2_PLACEMENT_3D ( 'NONE', #15098, #20726, #22678 ) ;
#19777=ORIENTED_EDGE ( 'NONE', *, *, #13728, .F. ) ;
#19858=ORIENTED_EDGE ( 'NONE', *, *, #5797, .F. ) ;
#19975=CARTESIAN_POINT ( 'NONE',  ( 0.000000000000000000, 0.000000000000000000, 0.000000000000000000 ) ) ;
#20037=PLANE ( 'NONE',  #9892 ) ;
#20042=DIRECTION ( 'NONE',  ( 0.000000000000000000, 0.000000000000000000, 1.000000000000000000 ) ) ;
#20068=VERTEX_POINT ( 'NONE', #18666 ) ;
#20122=VECTOR ( 'NONE', #4342, 1000.000000000000114 ) ;
#20248=CARTESIAN_POINT ( 'NONE',  ( 0.000000000000000000, 0.000000000000000000, 0.000000000000000000 ) ) ;
#20379=VERTEX_POINT ( 'NONE', #23541 ) ;
#20398=AXIS2_PLACEMENT_3D ( 'NONE', #20248, #22447, #11287 ) ;
#20726=DIRECTION ( 'NONE',  ( 0.000000000000000000, 0.000000000000000000, 1.000000000000000000 ) ) ;
#20856=FACE_OUTER_BOUND ( 'NONE', #675, .T. ) ;
#20898=ORIENTED_EDGE ( 'NONE', *, *, #9226, .F. ) ;
#20908=ORIENTED_EDGE ( 'NONE', *, *, #5300, .T. ) ;
#20922=PRODUCT_DEFINITION_CONTEXT ( 'detailed design', #13864, 'design' ) ;
#20943=LINE ( 'NONE', #4105, #552 ) ;
#21081=CARTESIAN_POINT ( 'NONE',  ( 0.000000000000000000, 0.000000000000000000, 15.50000000000000000 ) ) ;
#21093=DIRECTION ( 'NONE',  ( 1.000000000000000000, 0.000000000000000000, 0.000000000000000000 ) ) ;
#21119=CIRCLE ( 'NONE', #12536, 9.000000000000000000 ) ;
#21165=ORIENTED_EDGE ( 'NONE', *, *, #13728, .T. ) ;
#21207=CYLINDRICAL_SURFACE ( 'NONE', #23601, 9.000000000000000000 ) ;
#21391=CARTESIAN_POINT ( 'NONE',  ( 0.000000000000000000, 0.000000000000000000, 0.000000000000000000 ) ) ;
#21513=LINE ( 'NONE', #899, #11585 ) ;
#21641=DIRECTION ( 'NONE',  ( -0.000000000000000000, -0.000000000000000000, -1.000000000000000000 ) ) ;
#21761=CARTESIAN_POINT ( 'NONE',  ( 0.000000000000000000, 0.000000000000000000, 15.50000000000000000 ) ) ;
#21895=ORIENTED_EDGE ( 'NONE', *, *, #8347, .T. ) ;
#22016=CIRCLE ( 'NONE', #18116, 9.499999999999998224 ) ;
#22121=FACE_OUTER_BOUND ( 'NONE', #3787, .T. ) ;
#22314=DIRECTION ( 'NONE',  ( 0.000000000000000000, 0.000000000000000000, 1.000000000000000000 ) ) ;
#22318=DIRECTION ( 'NONE',  ( 1.000000000000000000, 0.000000000000000000, 0.000000000000000000 ) ) ;
#22344=DIRECTION ( 'NONE',  ( 0.000000000000000000, 0.000000000000000000, 1.000000000000000000 ) ) ;
#22447=DIRECTION ( 'NONE',  ( 0.000000000000000000, 0.000000000000000000, 1.000000000000000000 ) ) ;
#22502=EDGE_CURVE ( 'NONE', #17379, #13780, #13086, .T. ) ;
#22675=( LENGTH_UNIT ( ) NAMED_UNIT ( * ) SI_UNIT ( .MILLI., .METRE. ) );
#22676=DIRECTION ( 'NONE',  ( -1.000000000000000000, 0.000000000000000000, 0.000000000000000000 ) ) ;
#22678=DIRECTION ( 'NONE',  ( 1.000000000000000000, 0.000000000000000000, 0.000000000000000000 ) ) ;
#22826=DIRECTION ( 'NONE',  ( 0.000000000000000000, 0.000000000000000000, 1.000000000000000000 ) ) ;
#22841=EDGE_LOOP ( 'NONE', ( #1216, #18176 ) ) ;
#22861=EDGE_CURVE ( 'NONE', #20379, #16889, #17365, .T. ) ;
#22871=DIRECTION ( 'NONE',  ( 0.000000000000000000, 0.000000000000000000, 1.000000000000000000 ) ) ;
#22927=CARTESIAN_POINT ( 'NONE',  ( 9.999999999999998224, 1.224646799147353059E-15, 0.000000000000000000 ) ) ;
#22975=ORIENTED_EDGE ( 'NONE', *, *, #8875, .F. ) ;
#23045=DIRECTION ( 'NONE',  ( -0.000000000000000000, -0.000000000000000000, -1.000000000000000000 ) ) ;
#23222=CARTESIAN_POINT ( 'NONE',  ( 9.000000000000000000, 1.102182119232617714E-15, 15.00000000000000178 ) ) ;
#23477=CARTESIAN_POINT ( 'NONE',  ( 0.000000000000000000, 0.000000000000000000, 0.000000000000000000 ) ) ;
#23541=CARTESIAN_POINT ( 'NONE',  ( -9.999999999999998224, 0.000000000000000000, 0.000000000000000000 ) ) ;
#23588=EDGE_CURVE ( 'NONE', #13080, #15663, #12001, .T. ) ;
#23601=AXIS2_PLACEMENT_3D ( 'NONE', #2778, #2543, #11660 ) ;
#23620=ORIENTED_EDGE ( 'NONE', *, *, #4260, .F. ) ;
#23712=FACE_OUTER_BOUND ( 'NONE', #4557, .T. ) ;
#23858=AXIS2_PLACEMENT_3D ( 'NONE', #13902, #5966, #9610 ) ;
#23909=CIRCLE ( 'NONE', #18081, 9.999999999999998224 ) ;
#23931=ADVANCED_FACE ( 'NONE', ( #15505 ), #8832, .F. ) ;
#24135=COLOUR_RGB('Light Blue',0.38,0.62,0.78);
#24136=FILL_AREA_STYLE_COLOUR('',#24135);
#24137=FILL_AREA_STYLE('',(#24136));
#24138=SURFACE_STYLE_FILL_AREA(#24137);
#24139=SURFACE_SIDE_STYLE('',(#24138));
#24140=SURFACE_STYLE_USAGE(.BOTH.,#24139);
#24141=PRESENTATION_STYLE_ASSIGNMENT((#24140));
ENDSEC;
END-ISO-10303-21;
